ISO-10303-21;
HEADER;
/* Generated by software containing ST-Developer
 * from STEP Tools, Inc. (www.steptools.com) 
 */

FILE_DESCRIPTION(
/* description */ ('Hand-operated arbor press'),
/* implementation_level */ '2;1');

FILE_NAME(
/* name */ 'Socket Set Screw - M4x6.step',
/* time_stamp */ '2026-10-28T03:25:25-07:00',
/* author */ (''),
/* organization */ (''),
/* preprocessor_version */ 'ST-DEVELOPER v20.2',
/* originating_system */ 'Autodesk Translation Framework v15.17.0.0',
/* authorisation */ '');

FILE_SCHEMA (('AUTOMOTIVE_DESIGN { 1 0 10303 214 3 1 1 }'));
ENDSEC;

DATA;
#10=MECHANICAL_DESIGN_GEOMETRIC_PRESENTATION_REPRESENTATION('',(#618),#32751);
#488=CONICAL_SURFACE('',#13782,0.185,0.785398163397449);
#489=CONICAL_SURFACE('',#13786,0.1625,0.785398163397449);
#527=SHAPE_REPRESENTATION_RELATIONSHIP('SRR','None',#32958,#569);
#569=ADVANCED_BREP_SHAPE_REPRESENTATION('',(#665),#32732);
#618=STYLED_ITEM('',(#33249),#665);
#665=MANIFOLD_SOLID_BREP('Body1',#12517);
#816=FACE_BOUND('',#2587,.T.);
#1183=PLANE('',#13773);
#1184=PLANE('',#13774);
#1185=PLANE('',#13775);
#1186=PLANE('',#13776);
#1187=PLANE('',#13777);
#1188=PLANE('',#13778);
#1189=PLANE('',#13779);
#1190=PLANE('',#13780);
#1191=PLANE('',#13788);
#1762=FACE_OUTER_BOUND('',#2579,.T.);
#1763=FACE_OUTER_BOUND('',#2580,.T.);
#1764=FACE_OUTER_BOUND('',#2581,.T.);
#1765=FACE_OUTER_BOUND('',#2582,.T.);
#1766=FACE_OUTER_BOUND('',#2583,.T.);
#1767=FACE_OUTER_BOUND('',#2584,.T.);
#1768=FACE_OUTER_BOUND('',#2585,.T.);
#1769=FACE_OUTER_BOUND('',#2586,.T.);
#1770=FACE_OUTER_BOUND('',#2588,.T.);
#1771=FACE_OUTER_BOUND('',#2589,.T.);
#1772=FACE_OUTER_BOUND('',#2590,.T.);
#1773=FACE_OUTER_BOUND('',#2591,.T.);
#2579=EDGE_LOOP('',(#10672,#10673,#10674,#10675));
#2580=EDGE_LOOP('',(#10676,#10677,#10678,#10679));
#2581=EDGE_LOOP('',(#10680,#10681,#10682,#10683));
#2582=EDGE_LOOP('',(#10684,#10685,#10686,#10687));
#2583=EDGE_LOOP('',(#10688,#10689,#10690,#10691));
#2584=EDGE_LOOP('',(#10692,#10693,#10694,#10695));
#2585=EDGE_LOOP('',(#10696,#10697,#10698,#10699,#10700,#10701));
#2586=EDGE_LOOP('',(#10702));
#2587=EDGE_LOOP('',(#10703,#10704,#10705,#10706,#10707,#10708));
#2588=EDGE_LOOP('',(#10709,#10710,#10711,#10712));
#2589=EDGE_LOOP('',(#10713,#10714,#10715,#10716));
#2590=EDGE_LOOP('',(#10717,#10718,#10719,#10720));
#2591=EDGE_LOOP('',(#10721));
#3710=LINE('',#20470,#4881);
#3711=LINE('',#20472,#4882);
#3712=LINE('',#20474,#4883);
#3713=LINE('',#20475,#4884);
#3714=LINE('',#20478,#4885);
#3715=LINE('',#20480,#4886);
#3716=LINE('',#20481,#4887);
#3717=LINE('',#20484,#4888);
#3718=LINE('',#20486,#4889);
#3719=LINE('',#20487,#4890);
#3720=LINE('',#20490,#4891);
#3721=LINE('',#20492,#4892);
#3722=LINE('',#20493,#4893);
#3723=LINE('',#20496,#4894);
#3724=LINE('',#20498,#4895);
#3725=LINE('',#20499,#4896);
#3726=LINE('',#20501,#4897);
#3727=LINE('',#20502,#4898);
#3728=LINE('',#20510,#4899);
#3729=LINE('',#20514,#4900);
#3730=LINE('',#20518,#4901);
#4881=VECTOR('',#16591,1.);
#4882=VECTOR('',#16592,1.);
#4883=VECTOR('',#16593,1.);
#4884=VECTOR('',#16594,1.);
#4885=VECTOR('',#16597,1.);
#4886=VECTOR('',#16598,1.);
#4887=VECTOR('',#16599,1.);
#4888=VECTOR('',#16602,1.);
#4889=VECTOR('',#16603,1.);
#4890=VECTOR('',#16604,1.);
#4891=VECTOR('',#16607,1.);
#4892=VECTOR('',#16608,1.);
#4893=VECTOR('',#16609,1.);
#4894=VECTOR('',#16612,1.);
#4895=VECTOR('',#16613,1.);
#4896=VECTOR('',#16614,1.);
#4897=VECTOR('',#16617,1.);
#4898=VECTOR('',#16618,1.);
#4899=VECTOR('',#16629,0.185);
#4900=VECTOR('',#16634,0.2);
#4901=VECTOR('',#16639,0.1625);
#5436=CIRCLE('',#13781,0.17);
#5437=CIRCLE('',#13783,0.1954);
#5438=CIRCLE('',#13785,0.1954);
#5439=CIRCLE('',#13787,0.125);
#6345=VERTEX_POINT('',#20468);
#6346=VERTEX_POINT('',#20469);
#6347=VERTEX_POINT('',#20471);
#6348=VERTEX_POINT('',#20473);
#6349=VERTEX_POINT('',#20477);
#6350=VERTEX_POINT('',#20479);
#6351=VERTEX_POINT('',#20483);
#6352=VERTEX_POINT('',#20485);
#6353=VERTEX_POINT('',#20489);
#6354=VERTEX_POINT('',#20491);
#6355=VERTEX_POINT('',#20495);
#6356=VERTEX_POINT('',#20497);
#6357=VERTEX_POINT('',#20505);
#6358=VERTEX_POINT('',#20508);
#6359=VERTEX_POINT('',#20512);
#6360=VERTEX_POINT('',#20516);
#7839=EDGE_CURVE('',#6345,#6346,#3710,.T.);
#7840=EDGE_CURVE('',#6345,#6347,#3711,.T.);
#7841=EDGE_CURVE('',#6347,#6348,#3712,.T.);
#7842=EDGE_CURVE('',#6346,#6348,#3713,.T.);
#7843=EDGE_CURVE('',#6349,#6345,#3714,.T.);
#7844=EDGE_CURVE('',#6349,#6350,#3715,.T.);
#7845=EDGE_CURVE('',#6350,#6347,#3716,.T.);
#7846=EDGE_CURVE('',#6351,#6349,#3717,.T.);
#7847=EDGE_CURVE('',#6351,#6352,#3718,.T.);
#7848=EDGE_CURVE('',#6352,#6350,#3719,.T.);
#7849=EDGE_CURVE('',#6353,#6351,#3720,.T.);
#7850=EDGE_CURVE('',#6353,#6354,#3721,.T.);
#7851=EDGE_CURVE('',#6354,#6352,#3722,.T.);
#7852=EDGE_CURVE('',#6355,#6353,#3723,.T.);
#7853=EDGE_CURVE('',#6355,#6356,#3724,.T.);
#7854=EDGE_CURVE('',#6356,#6354,#3725,.T.);
#7855=EDGE_CURVE('',#6346,#6355,#3726,.T.);
#7856=EDGE_CURVE('',#6348,#6356,#3727,.T.);
#7857=EDGE_CURVE('',#6357,#6357,#5436,.T.);
#7858=EDGE_CURVE('',#6358,#6358,#5437,.T.);
#7859=EDGE_CURVE('',#6358,#6357,#3728,.T.);
#7860=EDGE_CURVE('',#6359,#6359,#5438,.F.);
#7861=EDGE_CURVE('',#6359,#6358,#3729,.T.);
#7862=EDGE_CURVE('',#6360,#6360,#5439,.T.);
#7863=EDGE_CURVE('',#6360,#6359,#3730,.T.);
#10672=ORIENTED_EDGE('',*,*,#7839,.F.);
#10673=ORIENTED_EDGE('',*,*,#7840,.T.);
#10674=ORIENTED_EDGE('',*,*,#7841,.T.);
#10675=ORIENTED_EDGE('',*,*,#7842,.F.);
#10676=ORIENTED_EDGE('',*,*,#7843,.F.);
#10677=ORIENTED_EDGE('',*,*,#7844,.T.);
#10678=ORIENTED_EDGE('',*,*,#7845,.T.);
#10679=ORIENTED_EDGE('',*,*,#7840,.F.);
#10680=ORIENTED_EDGE('',*,*,#7846,.F.);
#10681=ORIENTED_EDGE('',*,*,#7847,.T.);
#10682=ORIENTED_EDGE('',*,*,#7848,.T.);
#10683=ORIENTED_EDGE('',*,*,#7844,.F.);
#10684=ORIENTED_EDGE('',*,*,#7849,.F.);
#10685=ORIENTED_EDGE('',*,*,#7850,.T.);
#10686=ORIENTED_EDGE('',*,*,#7851,.T.);
#10687=ORIENTED_EDGE('',*,*,#7847,.F.);
#10688=ORIENTED_EDGE('',*,*,#7852,.F.);
#10689=ORIENTED_EDGE('',*,*,#7853,.T.);
#10690=ORIENTED_EDGE('',*,*,#7854,.T.);
#10691=ORIENTED_EDGE('',*,*,#7850,.F.);
#10692=ORIENTED_EDGE('',*,*,#7855,.F.);
#10693=ORIENTED_EDGE('',*,*,#7842,.T.);
#10694=ORIENTED_EDGE('',*,*,#7856,.T.);
#10695=ORIENTED_EDGE('',*,*,#7853,.F.);
#10696=ORIENTED_EDGE('',*,*,#7856,.F.);
#10697=ORIENTED_EDGE('',*,*,#7841,.F.);
#10698=ORIENTED_EDGE('',*,*,#7845,.F.);
#10699=ORIENTED_EDGE('',*,*,#7848,.F.);
#10700=ORIENTED_EDGE('',*,*,#7851,.F.);
#10701=ORIENTED_EDGE('',*,*,#7854,.F.);
#10702=ORIENTED_EDGE('',*,*,#7857,.F.);
#10703=ORIENTED_EDGE('',*,*,#7839,.T.);
#10704=ORIENTED_EDGE('',*,*,#7855,.T.);
#10705=ORIENTED_EDGE('',*,*,#7852,.T.);
#10706=ORIENTED_EDGE('',*,*,#7849,.T.);
#10707=ORIENTED_EDGE('',*,*,#7846,.T.);
#10708=ORIENTED_EDGE('',*,*,#7843,.T.);
#10709=ORIENTED_EDGE('',*,*,#7858,.F.);
#10710=ORIENTED_EDGE('',*,*,#7859,.T.);
#10711=ORIENTED_EDGE('',*,*,#7857,.T.);
#10712=ORIENTED_EDGE('',*,*,#7859,.F.);
#10713=ORIENTED_EDGE('',*,*,#7860,.F.);
#10714=ORIENTED_EDGE('',*,*,#7861,.T.);
#10715=ORIENTED_EDGE('',*,*,#7858,.T.);
#10716=ORIENTED_EDGE('',*,*,#7861,.F.);
#10717=ORIENTED_EDGE('',*,*,#7862,.F.);
#10718=ORIENTED_EDGE('',*,*,#7863,.T.);
#10719=ORIENTED_EDGE('',*,*,#7860,.T.);
#10720=ORIENTED_EDGE('',*,*,#7863,.F.);
#10721=ORIENTED_EDGE('',*,*,#7862,.T.);
#11750=CYLINDRICAL_SURFACE('',#13784,0.1954);
#12271=ADVANCED_FACE('',(#1762),#1183,.F.);
#12272=ADVANCED_FACE('',(#1763),#1184,.F.);
#12273=ADVANCED_FACE('',(#1764),#1185,.F.);
#12274=ADVANCED_FACE('',(#1765),#1186,.F.);
#12275=ADVANCED_FACE('',(#1766),#1187,.F.);
#12276=ADVANCED_FACE('',(#1767),#1188,.F.);
#12277=ADVANCED_FACE('',(#1768),#1189,.F.);
#12278=ADVANCED_FACE('',(#1769,#816),#1190,.T.);
#12279=ADVANCED_FACE('',(#1770),#488,.T.);
#12280=ADVANCED_FACE('',(#1771),#11750,.T.);
#12281=ADVANCED_FACE('',(#1772),#489,.T.);
#12282=ADVANCED_FACE('',(#1773),#1191,.T.);
#12517=CLOSED_SHELL('',(#12271,#12272,#12273,#12274,#12275,#12276,#12277,
#12278,#12279,#12280,#12281,#12282));
#13772=AXIS2_PLACEMENT_3D('',#20466,#16587,#16588);
#13773=AXIS2_PLACEMENT_3D('',#20467,#16589,#16590);
#13774=AXIS2_PLACEMENT_3D('',#20476,#16595,#16596);
#13775=AXIS2_PLACEMENT_3D('',#20482,#16600,#16601);
#13776=AXIS2_PLACEMENT_3D('',#20488,#16605,#16606);
#13777=AXIS2_PLACEMENT_3D('',#20494,#16610,#16611);
#13778=AXIS2_PLACEMENT_3D('',#20500,#16615,#16616);
#13779=AXIS2_PLACEMENT_3D('',#20503,#16619,#16620);
#13780=AXIS2_PLACEMENT_3D('',#20504,#16621,#16622);
#13781=AXIS2_PLACEMENT_3D('',#20506,#16623,#16624);
#13782=AXIS2_PLACEMENT_3D('',#20507,#16625,#16626);
#13783=AXIS2_PLACEMENT_3D('',#20509,#16627,#16628);
#13784=AXIS2_PLACEMENT_3D('',#20511,#16630,#16631);
#13785=AXIS2_PLACEMENT_3D('',#20513,#16632,#16633);
#13786=AXIS2_PLACEMENT_3D('',#20515,#16635,#16636);
#13787=AXIS2_PLACEMENT_3D('',#20517,#16637,#16638);
#13788=AXIS2_PLACEMENT_3D('',#20519,#16640,#16641);
#16587=DIRECTION('axis',(0.,0.,1.));
#16588=DIRECTION('refdir',(1.,0.,0.));
#16589=DIRECTION('center_axis',(0.866025403784439,0.,-0.5));
#16590=DIRECTION('ref_axis',(0.5,0.,0.866025403784439));
#16591=DIRECTION('',(0.5,0.,0.866025403784439));
#16592=DIRECTION('',(0.,-1.,0.));
#16593=DIRECTION('',(0.5,0.,0.866025403784439));
#16594=DIRECTION('',(0.,-1.,0.));
#16595=DIRECTION('center_axis',(1.20185167898973E-16,0.,-1.));
#16596=DIRECTION('ref_axis',(1.,0.,1.20185167898973E-16));
#16597=DIRECTION('',(1.,0.,1.20185167898973E-16));
#16598=DIRECTION('',(0.,-1.,0.));
#16599=DIRECTION('',(1.,0.,1.20185167898973E-16));
#16600=DIRECTION('center_axis',(-0.866025403784439,0.,-0.5));
#16601=DIRECTION('ref_axis',(0.5,0.,-0.866025403784439));
#16602=DIRECTION('',(0.5,0.,-0.866025403784439));
#16603=DIRECTION('',(0.,-1.,0.));
#16604=DIRECTION('',(0.5,0.,-0.866025403784439));
#16605=DIRECTION('center_axis',(-0.866025403784439,0.,0.5));
#16606=DIRECTION('ref_axis',(-0.5,0.,-0.866025403784439));
#16607=DIRECTION('',(-0.5,0.,-0.866025403784439));
#16608=DIRECTION('',(0.,-1.,0.));
#16609=DIRECTION('',(-0.5,0.,-0.866025403784439));
#16610=DIRECTION('center_axis',(-2.40370335797945E-16,0.,1.));
#16611=DIRECTION('ref_axis',(-1.,0.,-2.40370335797945E-16));
#16612=DIRECTION('',(-1.,0.,-2.40370335797945E-16));
#16613=DIRECTION('',(0.,-1.,0.));
#16614=DIRECTION('',(-1.,0.,-2.40370335797945E-16));
#16615=DIRECTION('center_axis',(0.866025403784439,0.,0.5));
#16616=DIRECTION('ref_axis',(-0.5,0.,0.866025403784439));
#16617=DIRECTION('',(-0.5,0.,0.866025403784439));
#16618=DIRECTION('',(-0.5,0.,0.866025403784439));
#16619=DIRECTION('center_axis',(0.,-1.,0.));
#16620=DIRECTION('ref_axis',(0.,0.,-1.));
#16621=DIRECTION('center_axis',(0.,1.,0.));
#16622=DIRECTION('ref_axis',(0.,0.,1.));
#16623=DIRECTION('center_axis',(0.,-1.,0.));
#16624=DIRECTION('ref_axis',(1.,0.,0.));
#16625=DIRECTION('center_axis',(0.,-1.,0.));
#16626=DIRECTION('ref_axis',(1.,0.,0.));
#16627=DIRECTION('center_axis',(0.,-1.,0.));
#16628=DIRECTION('ref_axis',(1.,0.,0.));
#16629=DIRECTION('',(0.707106781186548,0.707106781186547,8.65956056235494E-17));
#16630=DIRECTION('center_axis',(0.,-1.,0.));
#16631=DIRECTION('ref_axis',(1.,0.,0.));
#16632=DIRECTION('center_axis',(0.,1.,0.));
#16633=DIRECTION('ref_axis',(1.,0.,0.));
#16634=DIRECTION('',(0.,1.,0.));
#16635=DIRECTION('center_axis',(0.,1.,0.));
#16636=DIRECTION('ref_axis',(1.,0.,0.));
#16637=DIRECTION('center_axis',(0.,-1.,0.));
#16638=DIRECTION('ref_axis',(1.,0.,0.));
#16639=DIRECTION('',(-0.707106781186548,0.707106781186547,-8.65956056235494E-17));
#16640=DIRECTION('center_axis',(0.,-1.,0.));
#16641=DIRECTION('ref_axis',(0.,0.,-1.));
#20466=CARTESIAN_POINT('',(0.,0.,0.));
#20467=CARTESIAN_POINT('Origin',(0.0577350269189626,0.,-0.1));
#20468=CARTESIAN_POINT('',(0.0577350269189626,0.,-0.1));
#20469=CARTESIAN_POINT('',(0.115470053837925,0.,0.));
#20470=CARTESIAN_POINT('',(0.0934187836487032,0.,-0.0381939203391614));
#20471=CARTESIAN_POINT('',(0.0577350269189626,-0.2,-0.1));
#20472=CARTESIAN_POINT('',(0.0577350269189626,0.,-0.1));
#20473=CARTESIAN_POINT('',(0.115470053837925,-0.2,0.));
#20474=CARTESIAN_POINT('',(0.115470053837925,-0.2,0.));
#20475=CARTESIAN_POINT('',(0.115470053837925,0.,0.));
#20476=CARTESIAN_POINT('Origin',(-0.0577350269189626,0.,-0.1));
#20477=CARTESIAN_POINT('',(-0.0577350269189626,0.,-0.1));
#20478=CARTESIAN_POINT('',(0.0561324865405187,0.,-0.1));
#20479=CARTESIAN_POINT('',(-0.0577350269189626,-0.2,-0.1));
#20480=CARTESIAN_POINT('',(-0.0577350269189626,0.,-0.1));
#20481=CARTESIAN_POINT('',(0.0577350269189626,-0.2,-0.1));
#20482=CARTESIAN_POINT('Origin',(-0.115470053837925,0.,-1.38777878078145E-17));
#20483=CARTESIAN_POINT('',(-0.115470053837925,0.,-1.41410031829988E-17));
#20484=CARTESIAN_POINT('',(-0.0797862971081845,0.,-0.0618060796608387));
#20485=CARTESIAN_POINT('',(-0.115470053837925,-0.2,-1.38777878078145E-17));
#20486=CARTESIAN_POINT('',(-0.115470053837925,0.,-1.41410031829988E-17));
#20487=CARTESIAN_POINT('',(-0.0577350269189626,-0.2,-0.1));
#20488=CARTESIAN_POINT('Origin',(-0.0577350269189626,0.,0.1));
#20489=CARTESIAN_POINT('',(-0.0577350269189626,0.,0.1));
#20490=CARTESIAN_POINT('',(-0.0509187836487033,0.,0.111806079660839));
#20491=CARTESIAN_POINT('',(-0.0577350269189626,-0.2,0.1));
#20492=CARTESIAN_POINT('',(-0.0577350269189626,0.,0.1));
#20493=CARTESIAN_POINT('',(-0.115470053837925,-0.2,-1.41410031829988E-17));
#20494=CARTESIAN_POINT('Origin',(0.0577350269189626,0.,0.1));
#20495=CARTESIAN_POINT('',(0.0577350269189626,0.,0.1));
#20496=CARTESIAN_POINT('',(0.113867513459481,0.,0.1));
#20497=CARTESIAN_POINT('',(0.0577350269189626,-0.2,0.1));
#20498=CARTESIAN_POINT('',(0.0577350269189626,0.,0.1));
#20499=CARTESIAN_POINT('',(-0.0577350269189626,-0.2,0.1));
#20500=CARTESIAN_POINT('Origin',(0.115470053837925,0.,0.));
#20501=CARTESIAN_POINT('',(0.122286297108185,0.,-0.0118060796608386));
#20502=CARTESIAN_POINT('',(0.0577350269189626,-0.2,0.1));
#20503=CARTESIAN_POINT('Origin',(0.,-0.2,0.));
#20504=CARTESIAN_POINT('Origin',(0.17,0.,0.));
#20505=CARTESIAN_POINT('',(-0.17,-8.67361737988404E-18,-2.0818995585505E-17));
#20506=CARTESIAN_POINT('Origin',(0.,0.,0.));
#20507=CARTESIAN_POINT('Origin',(0.,-0.015,0.));
#20508=CARTESIAN_POINT('',(-0.1954,-0.0254,-2.39295984553393E-17));
#20509=CARTESIAN_POINT('Origin',(0.,-0.0254,0.));
#20510=CARTESIAN_POINT('',(-0.185,-0.015,-2.2655965784226E-17));
#20511=CARTESIAN_POINT('Origin',(0.,-0.2775,0.));
#20512=CARTESIAN_POINT('',(-0.1954,-0.5296,2.39295984553393E-17));
#20513=CARTESIAN_POINT('Origin',(0.,-0.5296,0.));
#20514=CARTESIAN_POINT('',(-0.1954,-0.2775,-2.39295984553393E-17));
#20515=CARTESIAN_POINT('Origin',(0.,-0.5625,0.));
#20516=CARTESIAN_POINT('',(-0.125,-0.6,-1.53080849893419E-17));
#20517=CARTESIAN_POINT('Origin',(0.,-0.6,0.));
#20518=CARTESIAN_POINT('',(-0.1625,-0.5625,-1.99005104861445E-17));
#20519=CARTESIAN_POINT('Origin',(0.,-0.6,0.));
#32683=UNCERTAINTY_MEASURE_WITH_UNIT(LENGTH_MEASURE(0.001),#32752,
'DISTANCE_ACCURACY_VALUE',
'Maximum model space distance between geometric entities at asserted c
onnectivities');
#32702=UNCERTAINTY_MEASURE_WITH_UNIT(LENGTH_MEASURE(0.001),#32752,
'DISTANCE_ACCURACY_VALUE',
'Maximum model space distance between geometric entities at asserted c
onnectivities');
#32732=(
GEOMETRIC_REPRESENTATION_CONTEXT(3)
GLOBAL_UNCERTAINTY_ASSIGNED_CONTEXT((#32683))
GLOBAL_UNIT_ASSIGNED_CONTEXT((#32752,#32754,#32755))
REPRESENTATION_CONTEXT('','3D')
);
#32751=(
GEOMETRIC_REPRESENTATION_CONTEXT(3)
GLOBAL_UNCERTAINTY_ASSIGNED_CONTEXT((#32702))
GLOBAL_UNIT_ASSIGNED_CONTEXT((#32752,#32754,#32755))
REPRESENTATION_CONTEXT('','3D')
);
#32752=(
LENGTH_UNIT()
NAMED_UNIT(*)
SI_UNIT(.CENTI.,.METRE.)
);
#32754=(
NAMED_UNIT(*)
PLANE_ANGLE_UNIT()
SI_UNIT($,.RADIAN.)
);
#32755=(
NAMED_UNIT(*)
SI_UNIT($,.STERADIAN.)
SOLID_ANGLE_UNIT()
);
#32785=SHAPE_DEFINITION_REPRESENTATION(#32838,#32958);
#32838=PRODUCT_DEFINITION_SHAPE('',$,#33007);
#32958=SHAPE_REPRESENTATION('',(#13772),#32732);
#32977=PRODUCT_DEFINITION_CONTEXT('part definition',#33123,'design');
#33007=PRODUCT_DEFINITION('Socket Set Screw - M4x6',
'Socket Set Screw - M4x6',#33055,#32977);
#33055=PRODUCT_DEFINITION_FORMATION('',$,#33154);
#33123=APPLICATION_CONTEXT(
'Core Data for Automotive Mechanical Design Process');
#33124=PRODUCT_CONTEXT('part definition',#33123,'mechanical');
#33154=PRODUCT('Socket Set Screw - M4x6','Socket Set Screw - M4x6',
'Socket Set Screw - M4x6',(#33124));
#33243=COLOUR_RGB('Black',0.12,0.14,0.17);
#33244=FILL_AREA_STYLE_COLOUR('',#33243);
#33245=FILL_AREA_STYLE('',(#33244));
#33246=SURFACE_STYLE_FILL_AREA(#33245);
#33247=SURFACE_SIDE_STYLE('',(#33246));
#33248=SURFACE_STYLE_USAGE(.BOTH.,#33247);
#33249=PRESENTATION_STYLE_ASSIGNMENT((#33248));
ENDSEC;
END-ISO-10303-21;
